ISO-10303-21;
HEADER;
/* Generated by software containing ST-Developer
 * from STEP Tools, Inc. (www.steptools.com) 
 */

FILE_DESCRIPTION(
/* description */ ('Bin tilter linkage'),
/* implementation_level */ '2;1');

FILE_NAME(
/* name */ 'M4 short cap screw (28).step',
/* time_stamp */ '2026-10-28T03:26:24-07:00',
/* author */ (''),
/* organization */ (''),
/* preprocessor_version */ 'ST-DEVELOPER v20.2',
/* originating_system */ 'Autodesk Translation Framework v15.17.0.0',
/* authorisation */ '');

FILE_SCHEMA (('AUTOMOTIVE_DESIGN { 1 0 10303 214 3 1 1 }'));
ENDSEC;

DATA;
#10=MECHANICAL_DESIGN_GEOMETRIC_PRESENTATION_REPRESENTATION('',(#930),#23728);
#718=SHAPE_REPRESENTATION_RELATIONSHIP('SRR','None',#24184,#824);
#824=ADVANCED_BREP_SHAPE_REPRESENTATION('',(#1043),#23684);
#930=STYLED_ITEM('',(#24772),#1043);
#1043=MANIFOLD_SOLID_BREP('Body1',#12461);
#1382=FACE_BOUND('',#3448,.T.);
#1725=PLANE('',#14734);
#1726=PLANE('',#14739);
#1727=PLANE('',#14742);
#2375=FACE_OUTER_BOUND('',#3447,.T.);
#2376=FACE_OUTER_BOUND('',#3449,.T.);
#2377=FACE_OUTER_BOUND('',#3450,.T.);
#2378=FACE_OUTER_BOUND('',#3451,.T.);
#2379=FACE_OUTER_BOUND('',#3452,.T.);
#3447=EDGE_LOOP('',(#10165));
#3448=EDGE_LOOP('',(#10166));
#3449=EDGE_LOOP('',(#10167,#10168,#10169,#10170));
#3450=EDGE_LOOP('',(#10171));
#3451=EDGE_LOOP('',(#10172,#10173,#10174,#10175));
#3452=EDGE_LOOP('',(#10176));
#4245=LINE('',#21803,#4920);
#4246=LINE('',#21807,#4921);
#4920=VECTOR('',#17996,0.350000000000001);
#4921=VECTOR('',#18001,0.199999999999999);
#5699=CIRCLE('',#14735,0.350000000000001);
#5700=CIRCLE('',#14736,0.199999999999999);
#5701=CIRCLE('',#14738,0.350000000000001);
#5702=CIRCLE('',#14741,0.199999999999999);
#6553=VERTEX_POINT('',#21796);
#6554=VERTEX_POINT('',#21798);
#6555=VERTEX_POINT('',#21801);
#6556=VERTEX_POINT('',#21806);
#7822=EDGE_CURVE('',#6553,#6553,#5699,.T.);
#7823=EDGE_CURVE('',#6554,#6554,#5700,.T.);
#7824=EDGE_CURVE('',#6555,#6555,#5701,.T.);
#7825=EDGE_CURVE('',#6555,#6553,#4245,.T.);
#7826=EDGE_CURVE('',#6554,#6556,#4246,.T.);
#7827=EDGE_CURVE('',#6556,#6556,#5702,.T.);
#10165=ORIENTED_EDGE('',*,*,#7822,.F.);
#10166=ORIENTED_EDGE('',*,*,#7823,.T.);
#10167=ORIENTED_EDGE('',*,*,#7824,.F.);
#10168=ORIENTED_EDGE('',*,*,#7825,.T.);
#10169=ORIENTED_EDGE('',*,*,#7822,.T.);
#10170=ORIENTED_EDGE('',*,*,#7825,.F.);
#10171=ORIENTED_EDGE('',*,*,#7824,.T.);
#10172=ORIENTED_EDGE('',*,*,#7823,.F.);
#10173=ORIENTED_EDGE('',*,*,#7826,.T.);
#10174=ORIENTED_EDGE('',*,*,#7827,.T.);
#10175=ORIENTED_EDGE('',*,*,#7826,.F.);
#10176=ORIENTED_EDGE('',*,*,#7827,.F.);
#11515=CYLINDRICAL_SURFACE('',#14737,0.350000000000001);
#11516=CYLINDRICAL_SURFACE('',#14740,0.199999999999999);
#12100=ADVANCED_FACE('',(#2375,#1382),#1725,.F.);
#12101=ADVANCED_FACE('',(#2376),#11515,.T.);
#12102=ADVANCED_FACE('',(#2377),#1726,.T.);
#12103=ADVANCED_FACE('',(#2378),#11516,.T.);
#12104=ADVANCED_FACE('',(#2379),#1727,.F.);
#12461=CLOSED_SHELL('',(#12100,#12101,#12102,#12103,#12104));
#14733=AXIS2_PLACEMENT_3D('',#21794,#17984,#17985);
#14734=AXIS2_PLACEMENT_3D('',#21795,#17986,#17987);
#14735=AXIS2_PLACEMENT_3D('',#21797,#17988,#17989);
#14736=AXIS2_PLACEMENT_3D('',#21799,#17990,#17991);
#14737=AXIS2_PLACEMENT_3D('',#21800,#17992,#17993);
#14738=AXIS2_PLACEMENT_3D('',#21802,#17994,#17995);
#14739=AXIS2_PLACEMENT_3D('',#21804,#17997,#17998);
#14740=AXIS2_PLACEMENT_3D('',#21805,#17999,#18000);
#14741=AXIS2_PLACEMENT_3D('',#21808,#18002,#18003);
#14742=AXIS2_PLACEMENT_3D('',#21809,#18004,#18005);
#17984=DIRECTION('axis',(0.,0.,1.));
#17985=DIRECTION('refdir',(1.,0.,0.));
#17986=DIRECTION('center_axis',(0.,1.,0.));
#17987=DIRECTION('ref_axis',(1.,0.,0.));
#17988=DIRECTION('center_axis',(0.,1.,0.));
#17989=DIRECTION('ref_axis',(1.,0.,0.));
#17990=DIRECTION('center_axis',(0.,1.,0.));
#17991=DIRECTION('ref_axis',(1.,0.,0.));
#17992=DIRECTION('center_axis',(0.,1.,0.));
#17993=DIRECTION('ref_axis',(1.,0.,0.));
#17994=DIRECTION('center_axis',(0.,1.,0.));
#17995=DIRECTION('ref_axis',(1.,0.,0.));
#17996=DIRECTION('',(0.,-1.,0.));
#17997=DIRECTION('center_axis',(0.,1.,0.));
#17998=DIRECTION('ref_axis',(1.,0.,0.));
#17999=DIRECTION('center_axis',(0.,1.,0.));
#18000=DIRECTION('ref_axis',(1.,0.,0.));
#18001=DIRECTION('',(0.,-1.,0.));
#18002=DIRECTION('center_axis',(0.,1.,0.));
#18003=DIRECTION('ref_axis',(1.,0.,0.));
#18004=DIRECTION('center_axis',(0.,1.,0.));
#18005=DIRECTION('ref_axis',(1.,0.,0.));
#21794=CARTESIAN_POINT('',(0.,0.,0.));
#21795=CARTESIAN_POINT('Origin',(25.5102260242172,0.8,29.9659007476824));
#21796=CARTESIAN_POINT('',(25.1602260242172,0.8,29.9659007476824));
#21797=CARTESIAN_POINT('Origin',(25.5102260242172,0.8,29.9659007476824));
#21798=CARTESIAN_POINT('',(25.3102260242172,0.8,29.9659007476824));
#21799=CARTESIAN_POINT('Origin',(25.5102260242172,0.8,29.9659007476824));
#21800=CARTESIAN_POINT('Origin',(25.5102260242172,0.8,29.9659007476824));
#21801=CARTESIAN_POINT('',(25.1602260242172,1.2,29.9659007476824));
#21802=CARTESIAN_POINT('Origin',(25.5102260242172,1.2,29.9659007476824));
#21803=CARTESIAN_POINT('',(25.1602260242172,0.8,29.9659007476824));
#21804=CARTESIAN_POINT('Origin',(25.5102260242172,1.2,29.9659007476824));
#21805=CARTESIAN_POINT('Origin',(25.5102260242172,0.1,29.9659007476824));
#21806=CARTESIAN_POINT('',(25.3102260242172,0.1,29.9659007476824));
#21807=CARTESIAN_POINT('',(25.3102260242172,0.1,29.9659007476824));
#21808=CARTESIAN_POINT('Origin',(25.5102260242172,0.1,29.9659007476824));
#21809=CARTESIAN_POINT('Origin',(25.5102260242172,0.1,29.9659007476824));
#23567=UNCERTAINTY_MEASURE_WITH_UNIT(LENGTH_MEASURE(0.001),#23729,
'DISTANCE_ACCURACY_VALUE',
'Maximum model space distance between geometric entities at asserted c
onnectivities');
#23611=UNCERTAINTY_MEASURE_WITH_UNIT(LENGTH_MEASURE(0.001),#23729,
'DISTANCE_ACCURACY_VALUE',
'Maximum model space distance between geometric entities at asserted c
onnectivities');
#23684=(
GEOMETRIC_REPRESENTATION_CONTEXT(3)
GLOBAL_UNCERTAINTY_ASSIGNED_CONTEXT((#23567))
GLOBAL_UNIT_ASSIGNED_CONTEXT((#23729,#23731,#23732))
REPRESENTATION_CONTEXT('','3D')
);
#23728=(
GEOMETRIC_REPRESENTATION_CONTEXT(3)
GLOBAL_UNCERTAINTY_ASSIGNED_CONTEXT((#23611))
GLOBAL_UNIT_ASSIGNED_CONTEXT((#23729,#23731,#23732))
REPRESENTATION_CONTEXT('','3D')
);
#23729=(
LENGTH_UNIT()
NAMED_UNIT(*)
SI_UNIT(.CENTI.,.METRE.)
);
#23731=(
NAMED_UNIT(*)
PLANE_ANGLE_UNIT()
SI_UNIT($,.RADIAN.)
);
#23732=(
NAMED_UNIT(*)
SI_UNIT($,.STERADIAN.)
SOLID_ANGLE_UNIT()
);
#23805=SHAPE_DEFINITION_REPRESENTATION(#23921,#24184);
#23921=PRODUCT_DEFINITION_SHAPE('',$,#24301);
#24184=SHAPE_REPRESENTATION('',(#14733),#23684);
#24228=PRODUCT_DEFINITION_CONTEXT('part definition',#24578,'design');
#24301=PRODUCT_DEFINITION('M4 short cap screw (28)',
'M4 short cap screw (28)',#24417,#24228);
#24417=PRODUCT_DEFINITION_FORMATION('',$,#24652);
#24578=APPLICATION_CONTEXT(
'Core Data for Automotive Mechanical Design Process');
#24579=PRODUCT_CONTEXT('part definition',#24578,'mechanical');
#24652=PRODUCT('M4 short cap screw (28)','M4 short cap screw (28)',
'M4 short cap screw (28)',(#24579));
#24766=COLOUR_RGB('Black',0.12,0.14,0.17);
#24767=FILL_AREA_STYLE_COLOUR('',#24766);
#24768=FILL_AREA_STYLE('',(#24767));
#24769=SURFACE_STYLE_FILL_AREA(#24768);
#24770=SURFACE_SIDE_STYLE('',(#24769));
#24771=SURFACE_STYLE_USAGE(.BOTH.,#24770);
#24772=PRESENTATION_STYLE_ASSIGNMENT((#24771));
ENDSEC;
END-ISO-10303-21;
